ISO-10303-21;
HEADER;
/* Generated by software containing ST-Developer
 * from STEP Tools, Inc. (www.steptools.com) 
 */

FILE_DESCRIPTION(
/* description */ ('Fatigue rig crank-slider'),
/* implementation_level */ '2;1');

FILE_NAME(
/* name */ 'M4x10 Cap Screw.step',
/* time_stamp */ '2026-10-28T03:24:50-07:00',
/* author */ (''),
/* organization */ (''),
/* preprocessor_version */ 'ST-DEVELOPER v20.2',
/* originating_system */ 'Autodesk Translation Framework v15.17.0.0',
/* authorisation */ '');

FILE_SCHEMA (('AUTOMOTIVE_DESIGN { 1 0 10303 214 3 1 1 }'));
ENDSEC;

DATA;
#10=MECHANICAL_DESIGN_GEOMETRIC_PRESENTATION_REPRESENTATION('',(#645),#16911);
#34=CONICAL_SURFACE('',#10517,0.325,0.785398163397448);
#35=CONICAL_SURFACE('',#10521,0.335,0.785398163397448);
#36=CONICAL_SURFACE('',#10525,0.21,0.463647609000806);
#41=ORIENTED_CLOSED_SHELL('',*,#8940,.F.);
#46=BREP_WITH_VOIDS('Body1',#8941,(#41));
#536=SHAPE_REPRESENTATION_RELATIONSHIP('SRR','None',#17181,#586);
#586=ADVANCED_BREP_SHAPE_REPRESENTATION('',(#46),#16910);
#645=STYLED_ITEM('',(#17494),#46);
#896=FACE_BOUND('',#2457,.T.);
#1206=PLANE('',#10505);
#1207=PLANE('',#10506);
#1208=PLANE('',#10507);
#1209=PLANE('',#10508);
#1210=PLANE('',#10509);
#1211=PLANE('',#10510);
#1212=PLANE('',#10511);
#1213=PLANE('',#10512);
#1214=PLANE('',#10513);
#1215=PLANE('',#10515);
#1216=PLANE('',#10523);
#1724=FACE_OUTER_BOUND('',#2443,.T.);
#1725=FACE_OUTER_BOUND('',#2444,.T.);
#1726=FACE_OUTER_BOUND('',#2445,.T.);
#1727=FACE_OUTER_BOUND('',#2446,.T.);
#1728=FACE_OUTER_BOUND('',#2447,.T.);
#1729=FACE_OUTER_BOUND('',#2448,.T.);
#1730=FACE_OUTER_BOUND('',#2449,.T.);
#1731=FACE_OUTER_BOUND('',#2450,.T.);
#1732=FACE_OUTER_BOUND('',#2451,.T.);
#1733=FACE_OUTER_BOUND('',#2452,.T.);
#1734=FACE_OUTER_BOUND('',#2453,.T.);
#1735=FACE_OUTER_BOUND('',#2454,.T.);
#1736=FACE_OUTER_BOUND('',#2455,.T.);
#1737=FACE_OUTER_BOUND('',#2456,.T.);
#1738=FACE_OUTER_BOUND('',#2458,.T.);
#1739=FACE_OUTER_BOUND('',#2459,.T.);
#2443=EDGE_LOOP('',(#8136,#8137,#8138,#8139));
#2444=EDGE_LOOP('',(#8140,#8141,#8142,#8143));
#2445=EDGE_LOOP('',(#8144,#8145,#8146,#8147));
#2446=EDGE_LOOP('',(#8148,#8149,#8150,#8151));
#2447=EDGE_LOOP('',(#8152,#8153,#8154,#8155));
#2448=EDGE_LOOP('',(#8156,#8157,#8158,#8159));
#2449=EDGE_LOOP('',(#8160,#8161,#8162,#8163,#8164,#8165));
#2450=EDGE_LOOP('',(#8166,#8167,#8168,#8169,#8170,#8171));
#2451=EDGE_LOOP('',(#8172));
#2452=EDGE_LOOP('',(#8173));
#2453=EDGE_LOOP('',(#8174,#8175,#8176,#8177));
#2454=EDGE_LOOP('',(#8178,#8179,#8180,#8181));
#2455=EDGE_LOOP('',(#8182,#8183,#8184,#8185));
#2456=EDGE_LOOP('',(#8186));
#2457=EDGE_LOOP('',(#8187));
#2458=EDGE_LOOP('',(#8188,#8189,#8190,#8191));
#2459=EDGE_LOOP('',(#8192,#8193,#8194,#8195));
#3083=LINE('',#16694,#3729);
#3084=LINE('',#16696,#3730);
#3085=LINE('',#16698,#3731);
#3086=LINE('',#16699,#3732);
#3087=LINE('',#16702,#3733);
#3088=LINE('',#16704,#3734);
#3089=LINE('',#16705,#3735);
#3090=LINE('',#16708,#3736);
#3091=LINE('',#16710,#3737);
#3092=LINE('',#16711,#3738);
#3093=LINE('',#16714,#3739);
#3094=LINE('',#16716,#3740);
#3095=LINE('',#16717,#3741);
#3096=LINE('',#16720,#3742);
#3097=LINE('',#16722,#3743);
#3098=LINE('',#16723,#3744);
#3099=LINE('',#16725,#3745);
#3100=LINE('',#16726,#3746);
#3101=LINE('',#16738,#3747);
#3102=LINE('',#16742,#3748);
#3103=LINE('',#16746,#3749);
#3104=LINE('',#16753,#3750);
#3105=LINE('',#16755,#3751);
#3729=VECTOR('',#13215,1.);
#3730=VECTOR('',#13216,1.);
#3731=VECTOR('',#13217,1.);
#3732=VECTOR('',#13218,1.);
#3733=VECTOR('',#13221,1.);
#3734=VECTOR('',#13222,1.);
#3735=VECTOR('',#13223,1.);
#3736=VECTOR('',#13226,1.);
#3737=VECTOR('',#13227,1.);
#3738=VECTOR('',#13228,1.);
#3739=VECTOR('',#13231,1.);
#3740=VECTOR('',#13232,1.);
#3741=VECTOR('',#13233,1.);
#3742=VECTOR('',#13236,1.);
#3743=VECTOR('',#13237,1.);
#3744=VECTOR('',#13238,1.);
#3745=VECTOR('',#13241,1.);
#3746=VECTOR('',#13242,1.);
#3747=VECTOR('',#13259,0.325);
#3748=VECTOR('',#13264,0.35);
#3749=VECTOR('',#13269,0.335);
#3750=VECTOR('',#13278,0.21);
#3751=VECTOR('',#13281,0.2);
#4145=CIRCLE('',#10514,0.1954);
#4146=CIRCLE('',#10516,0.3);
#4147=CIRCLE('',#10518,0.35);
#4148=CIRCLE('',#10520,0.35);
#4149=CIRCLE('',#10522,0.32);
#4150=CIRCLE('',#10524,0.22);
#4151=CIRCLE('',#10526,0.1954);
#4877=VERTEX_POINT('',#16692);
#4878=VERTEX_POINT('',#16693);
#4879=VERTEX_POINT('',#16695);
#4880=VERTEX_POINT('',#16697);
#4881=VERTEX_POINT('',#16701);
#4882=VERTEX_POINT('',#16703);
#4883=VERTEX_POINT('',#16707);
#4884=VERTEX_POINT('',#16709);
#4885=VERTEX_POINT('',#16713);
#4886=VERTEX_POINT('',#16715);
#4887=VERTEX_POINT('',#16719);
#4888=VERTEX_POINT('',#16721);
#4889=VERTEX_POINT('',#16730);
#4890=VERTEX_POINT('',#16733);
#4891=VERTEX_POINT('',#16736);
#4892=VERTEX_POINT('',#16740);
#4893=VERTEX_POINT('',#16744);
#4894=VERTEX_POINT('',#16748);
#4895=VERTEX_POINT('',#16751);
#5966=EDGE_CURVE('',#4877,#4878,#3083,.T.);
#5967=EDGE_CURVE('',#4878,#4879,#3084,.T.);
#5968=EDGE_CURVE('',#4879,#4880,#3085,.T.);
#5969=EDGE_CURVE('',#4877,#4880,#3086,.T.);
#5970=EDGE_CURVE('',#4878,#4881,#3087,.T.);
#5971=EDGE_CURVE('',#4881,#4882,#3088,.T.);
#5972=EDGE_CURVE('',#4882,#4879,#3089,.T.);
#5973=EDGE_CURVE('',#4881,#4883,#3090,.T.);
#5974=EDGE_CURVE('',#4883,#4884,#3091,.T.);
#5975=EDGE_CURVE('',#4884,#4882,#3092,.T.);
#5976=EDGE_CURVE('',#4883,#4885,#3093,.T.);
#5977=EDGE_CURVE('',#4885,#4886,#3094,.T.);
#5978=EDGE_CURVE('',#4886,#4884,#3095,.T.);
#5979=EDGE_CURVE('',#4885,#4887,#3096,.T.);
#5980=EDGE_CURVE('',#4887,#4888,#3097,.T.);
#5981=EDGE_CURVE('',#4888,#4886,#3098,.T.);
#5982=EDGE_CURVE('',#4887,#4877,#3099,.T.);
#5983=EDGE_CURVE('',#4880,#4888,#3100,.T.);
#5984=EDGE_CURVE('',#4889,#4889,#4145,.T.);
#5985=EDGE_CURVE('',#4890,#4890,#4146,.T.);
#5986=EDGE_CURVE('',#4891,#4891,#4147,.T.);
#5987=EDGE_CURVE('',#4891,#4890,#3101,.T.);
#5988=EDGE_CURVE('',#4892,#4892,#4148,.T.);
#5989=EDGE_CURVE('',#4892,#4891,#3102,.T.);
#5990=EDGE_CURVE('',#4893,#4893,#4149,.T.);
#5991=EDGE_CURVE('',#4893,#4892,#3103,.T.);
#5992=EDGE_CURVE('',#4894,#4894,#4150,.T.);
#5993=EDGE_CURVE('',#4895,#4895,#4151,.F.);
#5994=EDGE_CURVE('',#4895,#4894,#3104,.T.);
#5995=EDGE_CURVE('',#4889,#4895,#3105,.T.);
#8136=ORIENTED_EDGE('',*,*,#5966,.T.);
#8137=ORIENTED_EDGE('',*,*,#5967,.T.);
#8138=ORIENTED_EDGE('',*,*,#5968,.T.);
#8139=ORIENTED_EDGE('',*,*,#5969,.F.);
#8140=ORIENTED_EDGE('',*,*,#5970,.T.);
#8141=ORIENTED_EDGE('',*,*,#5971,.T.);
#8142=ORIENTED_EDGE('',*,*,#5972,.T.);
#8143=ORIENTED_EDGE('',*,*,#5967,.F.);
#8144=ORIENTED_EDGE('',*,*,#5973,.T.);
#8145=ORIENTED_EDGE('',*,*,#5974,.T.);
#8146=ORIENTED_EDGE('',*,*,#5975,.T.);
#8147=ORIENTED_EDGE('',*,*,#5971,.F.);
#8148=ORIENTED_EDGE('',*,*,#5976,.T.);
#8149=ORIENTED_EDGE('',*,*,#5977,.T.);
#8150=ORIENTED_EDGE('',*,*,#5978,.T.);
#8151=ORIENTED_EDGE('',*,*,#5974,.F.);
#8152=ORIENTED_EDGE('',*,*,#5979,.T.);
#8153=ORIENTED_EDGE('',*,*,#5980,.T.);
#8154=ORIENTED_EDGE('',*,*,#5981,.T.);
#8155=ORIENTED_EDGE('',*,*,#5977,.F.);
#8156=ORIENTED_EDGE('',*,*,#5982,.T.);
#8157=ORIENTED_EDGE('',*,*,#5969,.T.);
#8158=ORIENTED_EDGE('',*,*,#5983,.T.);
#8159=ORIENTED_EDGE('',*,*,#5980,.F.);
#8160=ORIENTED_EDGE('',*,*,#5982,.F.);
#8161=ORIENTED_EDGE('',*,*,#5979,.F.);
#8162=ORIENTED_EDGE('',*,*,#5976,.F.);
#8163=ORIENTED_EDGE('',*,*,#5973,.F.);
#8164=ORIENTED_EDGE('',*,*,#5970,.F.);
#8165=ORIENTED_EDGE('',*,*,#5966,.F.);
#8166=ORIENTED_EDGE('',*,*,#5983,.F.);
#8167=ORIENTED_EDGE('',*,*,#5968,.F.);
#8168=ORIENTED_EDGE('',*,*,#5972,.F.);
#8169=ORIENTED_EDGE('',*,*,#5975,.F.);
#8170=ORIENTED_EDGE('',*,*,#5978,.F.);
#8171=ORIENTED_EDGE('',*,*,#5981,.F.);
#8172=ORIENTED_EDGE('',*,*,#5984,.F.);
#8173=ORIENTED_EDGE('',*,*,#5985,.F.);
#8174=ORIENTED_EDGE('',*,*,#5986,.F.);
#8175=ORIENTED_EDGE('',*,*,#5987,.T.);
#8176=ORIENTED_EDGE('',*,*,#5985,.T.);
#8177=ORIENTED_EDGE('',*,*,#5987,.F.);
#8178=ORIENTED_EDGE('',*,*,#5988,.F.);
#8179=ORIENTED_EDGE('',*,*,#5989,.T.);
#8180=ORIENTED_EDGE('',*,*,#5986,.T.);
#8181=ORIENTED_EDGE('',*,*,#5989,.F.);
#8182=ORIENTED_EDGE('',*,*,#5990,.F.);
#8183=ORIENTED_EDGE('',*,*,#5991,.T.);
#8184=ORIENTED_EDGE('',*,*,#5988,.T.);
#8185=ORIENTED_EDGE('',*,*,#5991,.F.);
#8186=ORIENTED_EDGE('',*,*,#5990,.T.);
#8187=ORIENTED_EDGE('',*,*,#5992,.F.);
#8188=ORIENTED_EDGE('',*,*,#5993,.F.);
#8189=ORIENTED_EDGE('',*,*,#5994,.T.);
#8190=ORIENTED_EDGE('',*,*,#5992,.T.);
#8191=ORIENTED_EDGE('',*,*,#5994,.F.);
#8192=ORIENTED_EDGE('',*,*,#5984,.T.);
#8193=ORIENTED_EDGE('',*,*,#5995,.T.);
#8194=ORIENTED_EDGE('',*,*,#5993,.T.);
#8195=ORIENTED_EDGE('',*,*,#5995,.F.);
#8353=CYLINDRICAL_SURFACE('',#10519,0.35);
#8354=CYLINDRICAL_SURFACE('',#10527,0.1954);
#8862=ADVANCED_FACE('',(#1724),#1206,.F.);
#8863=ADVANCED_FACE('',(#1725),#1207,.F.);
#8864=ADVANCED_FACE('',(#1726),#1208,.F.);
#8865=ADVANCED_FACE('',(#1727),#1209,.F.);
#8866=ADVANCED_FACE('',(#1728),#1210,.F.);
#8867=ADVANCED_FACE('',(#1729),#1211,.F.);
#8868=ADVANCED_FACE('',(#1730),#1212,.F.);
#8869=ADVANCED_FACE('',(#1731),#1213,.F.);
#8870=ADVANCED_FACE('',(#1732),#1214,.F.);
#8871=ADVANCED_FACE('',(#1733),#1215,.T.);
#8872=ADVANCED_FACE('',(#1734),#34,.T.);
#8873=ADVANCED_FACE('',(#1735),#8353,.T.);
#8874=ADVANCED_FACE('',(#1736),#35,.T.);
#8875=ADVANCED_FACE('',(#1737,#896),#1216,.T.);
#8876=ADVANCED_FACE('',(#1738),#36,.T.);
#8877=ADVANCED_FACE('',(#1739),#8354,.T.);
#8940=CLOSED_SHELL('',(#8862,#8863,#8864,#8865,#8866,#8867,#8868,#8869));
#8941=CLOSED_SHELL('',(#8870,#8871,#8872,#8873,#8874,#8875,#8876,#8877));
#10504=AXIS2_PLACEMENT_3D('',#16690,#13211,#13212);
#10505=AXIS2_PLACEMENT_3D('',#16691,#13213,#13214);
#10506=AXIS2_PLACEMENT_3D('',#16700,#13219,#13220);
#10507=AXIS2_PLACEMENT_3D('',#16706,#13224,#13225);
#10508=AXIS2_PLACEMENT_3D('',#16712,#13229,#13230);
#10509=AXIS2_PLACEMENT_3D('',#16718,#13234,#13235);
#10510=AXIS2_PLACEMENT_3D('',#16724,#13239,#13240);
#10511=AXIS2_PLACEMENT_3D('',#16727,#13243,#13244);
#10512=AXIS2_PLACEMENT_3D('',#16728,#13245,#13246);
#10513=AXIS2_PLACEMENT_3D('',#16729,#13247,#13248);
#10514=AXIS2_PLACEMENT_3D('',#16731,#13249,#13250);
#10515=AXIS2_PLACEMENT_3D('',#16732,#13251,#13252);
#10516=AXIS2_PLACEMENT_3D('',#16734,#13253,#13254);
#10517=AXIS2_PLACEMENT_3D('',#16735,#13255,#13256);
#10518=AXIS2_PLACEMENT_3D('',#16737,#13257,#13258);
#10519=AXIS2_PLACEMENT_3D('',#16739,#13260,#13261);
#10520=AXIS2_PLACEMENT_3D('',#16741,#13262,#13263);
#10521=AXIS2_PLACEMENT_3D('',#16743,#13265,#13266);
#10522=AXIS2_PLACEMENT_3D('',#16745,#13267,#13268);
#10523=AXIS2_PLACEMENT_3D('',#16747,#13270,#13271);
#10524=AXIS2_PLACEMENT_3D('',#16749,#13272,#13273);
#10525=AXIS2_PLACEMENT_3D('',#16750,#13274,#13275);
#10526=AXIS2_PLACEMENT_3D('',#16752,#13276,#13277);
#10527=AXIS2_PLACEMENT_3D('',#16754,#13279,#13280);
#13211=DIRECTION('axis',(0.,0.,1.));
#13212=DIRECTION('refdir',(1.,0.,0.));
#13213=DIRECTION('center_axis',(0.866025403784439,0.,-0.5));
#13214=DIRECTION('ref_axis',(0.5,0.,0.866025403784439));
#13215=DIRECTION('',(-0.5,0.,-0.866025403784439));
#13216=DIRECTION('',(0.,-1.,0.));
#13217=DIRECTION('',(0.5,0.,0.866025403784439));
#13218=DIRECTION('',(0.,-1.,0.));
#13219=DIRECTION('center_axis',(1.60246890531964E-16,0.,-1.));
#13220=DIRECTION('ref_axis',(1.,0.,1.60246890531964E-16));
#13221=DIRECTION('',(-1.,0.,-1.60246890531964E-16));
#13222=DIRECTION('',(0.,-1.,0.));
#13223=DIRECTION('',(1.,0.,1.60246890531964E-16));
#13224=DIRECTION('center_axis',(-0.866025403784439,0.,-0.5));
#13225=DIRECTION('ref_axis',(0.5,0.,-0.866025403784439));
#13226=DIRECTION('',(-0.5,0.,0.866025403784439));
#13227=DIRECTION('',(0.,-1.,0.));
#13228=DIRECTION('',(0.5,0.,-0.866025403784439));
#13229=DIRECTION('center_axis',(-0.866025403784439,0.,0.5));
#13230=DIRECTION('ref_axis',(-0.5,0.,-0.866025403784439));
#13231=DIRECTION('',(0.5,0.,0.866025403784439));
#13232=DIRECTION('',(0.,-1.,0.));
#13233=DIRECTION('',(-0.5,0.,-0.866025403784439));
#13234=DIRECTION('center_axis',(-1.60246890531964E-16,0.,1.));
#13235=DIRECTION('ref_axis',(-1.,0.,-1.60246890531964E-16));
#13236=DIRECTION('',(1.,0.,1.60246890531964E-16));
#13237=DIRECTION('',(0.,-1.,0.));
#13238=DIRECTION('',(-1.,0.,-1.60246890531964E-16));
#13239=DIRECTION('center_axis',(0.866025403784439,0.,0.5));
#13240=DIRECTION('ref_axis',(-0.5,0.,0.866025403784439));
#13241=DIRECTION('',(0.5,0.,-0.866025403784439));
#13242=DIRECTION('',(-0.5,0.,0.866025403784439));
#13243=DIRECTION('center_axis',(0.,1.,0.));
#13244=DIRECTION('ref_axis',(1.,0.,0.));
#13245=DIRECTION('center_axis',(0.,-1.,0.));
#13246=DIRECTION('ref_axis',(0.,0.,-1.));
#13247=DIRECTION('center_axis',(0.,1.,0.));
#13248=DIRECTION('ref_axis',(1.,0.,0.));
#13249=DIRECTION('center_axis',(0.,1.,0.));
#13250=DIRECTION('ref_axis',(1.,0.,0.));
#13251=DIRECTION('center_axis',(0.,1.,0.));
#13252=DIRECTION('ref_axis',(0.,0.,1.));
#13253=DIRECTION('center_axis',(0.,-1.,0.));
#13254=DIRECTION('ref_axis',(1.,0.,0.));
#13255=DIRECTION('center_axis',(0.,-1.,0.));
#13256=DIRECTION('ref_axis',(1.,0.,0.));
#13257=DIRECTION('center_axis',(0.,-1.,0.));
#13258=DIRECTION('ref_axis',(1.,0.,0.));
#13259=DIRECTION('',(0.707106781186547,0.707106781186548,8.65956056235493E-17));
#13260=DIRECTION('center_axis',(0.,-1.,0.));
#13261=DIRECTION('ref_axis',(1.,0.,0.));
#13262=DIRECTION('center_axis',(0.,-1.,0.));
#13263=DIRECTION('ref_axis',(1.,0.,0.));
#13264=DIRECTION('',(0.,1.,0.));
#13265=DIRECTION('center_axis',(0.,1.,0.));
#13266=DIRECTION('ref_axis',(1.,0.,0.));
#13267=DIRECTION('center_axis',(0.,-1.,0.));
#13268=DIRECTION('ref_axis',(1.,0.,0.));
#13269=DIRECTION('',(-0.707106781186547,0.707106781186548,-8.65956056235493E-17));
#13270=DIRECTION('center_axis',(0.,-1.,0.));
#13271=DIRECTION('ref_axis',(0.,0.,-1.));
#13272=DIRECTION('center_axis',(0.,-1.,0.));
#13273=DIRECTION('ref_axis',(1.,0.,0.));
#13274=DIRECTION('center_axis',(0.,1.,0.));
#13275=DIRECTION('ref_axis',(1.,0.,0.));
#13276=DIRECTION('center_axis',(0.,1.,0.));
#13277=DIRECTION('ref_axis',(1.,0.,0.));
#13278=DIRECTION('',(-0.447213595499958,0.894427190999916,-5.47678698264203E-17));
#13279=DIRECTION('center_axis',(0.,-1.,0.));
#13280=DIRECTION('ref_axis',(1.,0.,0.));
#13281=DIRECTION('',(0.,1.,0.));
#16690=CARTESIAN_POINT('',(0.,0.,0.));
#16691=CARTESIAN_POINT('Origin',(0.0866025403784439,-0.4,-0.15));
#16692=CARTESIAN_POINT('',(0.173205080756888,-0.4,0.));
#16693=CARTESIAN_POINT('',(0.0866025403784439,-0.4,-0.15));
#16694=CARTESIAN_POINT('',(0.173205080756888,-0.4,0.));
#16695=CARTESIAN_POINT('',(0.0866025403784439,-0.64,-0.15));
#16696=CARTESIAN_POINT('',(0.0866025403784439,-0.4,-0.15));
#16697=CARTESIAN_POINT('',(0.173205080756888,-0.64,0.));
#16698=CARTESIAN_POINT('',(0.173205080756888,-0.64,0.));
#16699=CARTESIAN_POINT('',(0.173205080756888,-0.4,0.));
#16700=CARTESIAN_POINT('Origin',(-0.0866025403784438,-0.4,-0.15));
#16701=CARTESIAN_POINT('',(-0.0866025403784438,-0.4,-0.15));
#16702=CARTESIAN_POINT('',(0.0866025403784439,-0.4,-0.15));
#16703=CARTESIAN_POINT('',(-0.0866025403784438,-0.64,-0.15));
#16704=CARTESIAN_POINT('',(-0.0866025403784438,-0.4,-0.15));
#16705=CARTESIAN_POINT('',(0.0866025403784439,-0.64,-0.15));
#16706=CARTESIAN_POINT('Origin',(-0.173205080756888,-0.4,-2.77555756156289E-17));
#16707=CARTESIAN_POINT('',(-0.173205080756888,-0.4,-2.12115047744981E-17));
#16708=CARTESIAN_POINT('',(-0.0866025403784438,-0.4,-0.15));
#16709=CARTESIAN_POINT('',(-0.173205080756888,-0.64,-2.77555756156289E-17));
#16710=CARTESIAN_POINT('',(-0.173205080756888,-0.4,-2.12115047744981E-17));
#16711=CARTESIAN_POINT('',(-0.0866025403784438,-0.64,-0.15));
#16712=CARTESIAN_POINT('Origin',(-0.0866025403784439,-0.4,0.15));
#16713=CARTESIAN_POINT('',(-0.0866025403784439,-0.4,0.15));
#16714=CARTESIAN_POINT('',(-0.173205080756888,-0.4,-2.12115047744981E-17));
#16715=CARTESIAN_POINT('',(-0.0866025403784439,-0.64,0.15));
#16716=CARTESIAN_POINT('',(-0.0866025403784439,-0.4,0.15));
#16717=CARTESIAN_POINT('',(-0.173205080756888,-0.64,-2.12115047744981E-17));
#16718=CARTESIAN_POINT('Origin',(0.0866025403784439,-0.4,0.15));
#16719=CARTESIAN_POINT('',(0.0866025403784439,-0.4,0.15));
#16720=CARTESIAN_POINT('',(-0.0866025403784439,-0.4,0.15));
#16721=CARTESIAN_POINT('',(0.0866025403784439,-0.64,0.15));
#16722=CARTESIAN_POINT('',(0.0866025403784439,-0.4,0.15));
#16723=CARTESIAN_POINT('',(-0.0866025403784439,-0.64,0.15));
#16724=CARTESIAN_POINT('Origin',(0.173205080756888,-0.4,0.));
#16725=CARTESIAN_POINT('',(0.0866025403784439,-0.4,0.15));
#16726=CARTESIAN_POINT('',(0.0866025403784439,-0.64,0.15));
#16727=CARTESIAN_POINT('Origin',(0.,-0.4,-2.77555756156289E-17));
#16728=CARTESIAN_POINT('Origin',(0.,-0.64,-2.77555756156289E-17));
#16729=CARTESIAN_POINT('Origin',(0.,-1.,0.));
#16730=CARTESIAN_POINT('',(-0.1954,-1.,2.39295984553393E-17));
#16731=CARTESIAN_POINT('Origin',(0.,-1.,0.));
#16732=CARTESIAN_POINT('Origin',(0.3,0.4,0.));
#16733=CARTESIAN_POINT('',(-0.3,0.4,-3.67394039744206E-17));
#16734=CARTESIAN_POINT('Origin',(0.,0.4,0.));
#16735=CARTESIAN_POINT('Origin',(0.,0.375,0.));
#16736=CARTESIAN_POINT('',(-0.35,0.35,-4.28626379701573E-17));
#16737=CARTESIAN_POINT('Origin',(0.,0.35,0.));
#16738=CARTESIAN_POINT('',(-0.325,0.375,-3.9801020972289E-17));
#16739=CARTESIAN_POINT('Origin',(0.,0.19,0.));
#16740=CARTESIAN_POINT('',(-0.35,0.03,-4.28626379701574E-17));
#16741=CARTESIAN_POINT('Origin',(0.,0.03,0.));
#16742=CARTESIAN_POINT('',(-0.35,0.19,-4.28626379701574E-17));
#16743=CARTESIAN_POINT('Origin',(0.,0.0149999999999999,0.));
#16744=CARTESIAN_POINT('',(-0.32,-3.29597460435593E-17,-3.91886975727153E-17));
#16745=CARTESIAN_POINT('Origin',(0.,0.,0.));
#16746=CARTESIAN_POINT('',(-0.335,0.0149999999999999,-4.10256677714363E-17));
#16747=CARTESIAN_POINT('Origin',(0.22,0.,0.));
#16748=CARTESIAN_POINT('',(-0.22,-6.93889390390723E-18,-2.69422295812418E-17));
#16749=CARTESIAN_POINT('Origin',(0.,0.,0.));
#16750=CARTESIAN_POINT('Origin',(0.,-0.02,0.));
#16751=CARTESIAN_POINT('',(-0.1954,-0.0492,2.39295984553393E-17));
#16752=CARTESIAN_POINT('Origin',(0.,-0.0492,0.));
#16753=CARTESIAN_POINT('',(-0.21,-0.02,-2.57175827820944E-17));
#16754=CARTESIAN_POINT('Origin',(0.,-0.8,0.));
#16755=CARTESIAN_POINT('',(-0.1954,-0.8,-2.39295984553393E-17));
#16851=UNCERTAINTY_MEASURE_WITH_UNIT(LENGTH_MEASURE(0.001),#16912,
'DISTANCE_ACCURACY_VALUE',
'Maximum model space distance between geometric entities at asserted c
onnectivities');
#16852=UNCERTAINTY_MEASURE_WITH_UNIT(LENGTH_MEASURE(0.001),#16912,
'DISTANCE_ACCURACY_VALUE',
'Maximum model space distance between geometric entities at asserted c
onnectivities');
#16910=(
GEOMETRIC_REPRESENTATION_CONTEXT(3)
GLOBAL_UNCERTAINTY_ASSIGNED_CONTEXT((#16851))
GLOBAL_UNIT_ASSIGNED_CONTEXT((#16912,#16914,#16915))
REPRESENTATION_CONTEXT('','3D')
);
#16911=(
GEOMETRIC_REPRESENTATION_CONTEXT(3)
GLOBAL_UNCERTAINTY_ASSIGNED_CONTEXT((#16852))
GLOBAL_UNIT_ASSIGNED_CONTEXT((#16912,#16914,#16915))
REPRESENTATION_CONTEXT('','3D')
);
#16912=(
LENGTH_UNIT()
NAMED_UNIT(*)
SI_UNIT(.CENTI.,.METRE.)
);
#16914=(
NAMED_UNIT(*)
PLANE_ANGLE_UNIT()
SI_UNIT($,.RADIAN.)
);
#16915=(
NAMED_UNIT(*)
SI_UNIT($,.STERADIAN.)
SOLID_ANGLE_UNIT()
);
#16973=SHAPE_DEFINITION_REPRESENTATION(#17085,#17181);
#17085=PRODUCT_DEFINITION_SHAPE('',$,#17240);
#17181=SHAPE_REPRESENTATION('',(#10504),#16910);
#17182=PRODUCT_DEFINITION_CONTEXT('part definition',#17358,'design');
#17240=PRODUCT_DEFINITION('M4x10 Cap Screw','M4x10 Cap Screw',#17298,#17182);
#17298=PRODUCT_DEFINITION_FORMATION('',$,#17417);
#17358=APPLICATION_CONTEXT(
'Core Data for Automotive Mechanical Design Process');
#17359=PRODUCT_CONTEXT('part definition',#17358,'mechanical');
#17417=PRODUCT('M4x10 Cap Screw','M4x10 Cap Screw','M4x10 Cap Screw',(#17359));
#17488=COLOUR_RGB('Black',0.12,0.14,0.17);
#17489=FILL_AREA_STYLE_COLOUR('',#17488);
#17490=FILL_AREA_STYLE('',(#17489));
#17491=SURFACE_STYLE_FILL_AREA(#17490);
#17492=SURFACE_SIDE_STYLE('',(#17491));
#17493=SURFACE_STYLE_USAGE(.BOTH.,#17492);
#17494=PRESENTATION_STYLE_ASSIGNMENT((#17493));
ENDSEC;
END-ISO-10303-21;
